ISO-10303-21;
HEADER;
/* Generated by software containing ST-Developer
 * from STEP Tools, Inc. (www.steptools.com) 
 */

FILE_DESCRIPTION(
/* description */ ('Flywheel Crank-Slider'),
/* implementation_level */ '2;1');

FILE_NAME(
/* name */ 'Socket Set Screw - M5x8.step',
/* time_stamp */ '2026-10-28T03:23:13-07:00',
/* author */ (''),
/* organization */ (''),
/* preprocessor_version */ 'ST-DEVELOPER v20.2',
/* originating_system */ 'Autodesk Translation Framework v15.17.0.0',
/* authorisation */ '');

FILE_SCHEMA (('AUTOMOTIVE_DESIGN { 1 0 10303 214 3 1 1 }'));
ENDSEC;

DATA;
#10=MECHANICAL_DESIGN_GEOMETRIC_PRESENTATION_REPRESENTATION('',(#700),#17322);
#550=CONICAL_SURFACE('',#10332,0.235,0.785398163397448);
#551=CONICAL_SURFACE('',#10336,0.2125,0.785398163397448);
#595=SHAPE_REPRESENTATION_RELATIONSHIP('SRR','None',#17593,#647);
#647=ADVANCED_BREP_SHAPE_REPRESENTATION('',(#757),#17297);
#700=STYLED_ITEM('',(#17938),#757);
#757=MANIFOLD_SOLID_BREP('Body1',#9082);
#930=FACE_BOUND('',#2354,.T.);
#1221=PLANE('',#10323);
#1222=PLANE('',#10324);
#1223=PLANE('',#10325);
#1224=PLANE('',#10326);
#1225=PLANE('',#10327);
#1226=PLANE('',#10328);
#1227=PLANE('',#10329);
#1228=PLANE('',#10330);
#1229=PLANE('',#10338);
#1666=FACE_OUTER_BOUND('',#2346,.T.);
#1667=FACE_OUTER_BOUND('',#2347,.T.);
#1668=FACE_OUTER_BOUND('',#2348,.T.);
#1669=FACE_OUTER_BOUND('',#2349,.T.);
#1670=FACE_OUTER_BOUND('',#2350,.T.);
#1671=FACE_OUTER_BOUND('',#2351,.T.);
#1672=FACE_OUTER_BOUND('',#2352,.T.);
#1673=FACE_OUTER_BOUND('',#2353,.T.);
#1674=FACE_OUTER_BOUND('',#2355,.T.);
#1675=FACE_OUTER_BOUND('',#2356,.T.);
#1676=FACE_OUTER_BOUND('',#2357,.T.);
#1677=FACE_OUTER_BOUND('',#2358,.T.);
#2346=EDGE_LOOP('',(#7564,#7565,#7566,#7567));
#2347=EDGE_LOOP('',(#7568,#7569,#7570,#7571));
#2348=EDGE_LOOP('',(#7572,#7573,#7574,#7575));
#2349=EDGE_LOOP('',(#7576,#7577,#7578,#7579));
#2350=EDGE_LOOP('',(#7580,#7581,#7582,#7583));
#2351=EDGE_LOOP('',(#7584,#7585,#7586,#7587));
#2352=EDGE_LOOP('',(#7588,#7589,#7590,#7591,#7592,#7593));
#2353=EDGE_LOOP('',(#7594));
#2354=EDGE_LOOP('',(#7595,#7596,#7597,#7598,#7599,#7600));
#2355=EDGE_LOOP('',(#7601,#7602,#7603,#7604));
#2356=EDGE_LOOP('',(#7605,#7606,#7607,#7608));
#2357=EDGE_LOOP('',(#7609,#7610,#7611,#7612));
#2358=EDGE_LOOP('',(#7613));
#3047=LINE('',#15898,#3658);
#3048=LINE('',#15900,#3659);
#3049=LINE('',#15902,#3660);
#3050=LINE('',#15903,#3661);
#3051=LINE('',#15906,#3662);
#3052=LINE('',#15908,#3663);
#3053=LINE('',#15909,#3664);
#3054=LINE('',#15912,#3665);
#3055=LINE('',#15914,#3666);
#3056=LINE('',#15915,#3667);
#3057=LINE('',#15918,#3668);
#3058=LINE('',#15920,#3669);
#3059=LINE('',#15921,#3670);
#3060=LINE('',#15924,#3671);
#3061=LINE('',#15926,#3672);
#3062=LINE('',#15927,#3673);
#3063=LINE('',#15929,#3674);
#3064=LINE('',#15930,#3675);
#3065=LINE('',#15938,#3676);
#3066=LINE('',#15942,#3677);
#3067=LINE('',#15946,#3678);
#3658=VECTOR('',#12539,1.);
#3659=VECTOR('',#12540,1.);
#3660=VECTOR('',#12541,1.);
#3661=VECTOR('',#12542,1.);
#3662=VECTOR('',#12545,1.);
#3663=VECTOR('',#12546,1.);
#3664=VECTOR('',#12547,1.);
#3665=VECTOR('',#12550,1.);
#3666=VECTOR('',#12551,1.);
#3667=VECTOR('',#12552,1.);
#3668=VECTOR('',#12555,1.);
#3669=VECTOR('',#12556,1.);
#3670=VECTOR('',#12557,1.);
#3671=VECTOR('',#12560,1.);
#3672=VECTOR('',#12561,1.);
#3673=VECTOR('',#12562,1.);
#3674=VECTOR('',#12565,1.);
#3675=VECTOR('',#12566,1.);
#3676=VECTOR('',#12577,0.235);
#3677=VECTOR('',#12582,0.25);
#3678=VECTOR('',#12587,0.2125);
#4092=CIRCLE('',#10331,0.22);
#4093=CIRCLE('',#10333,0.24505);
#4094=CIRCLE('',#10335,0.24505);
#4095=CIRCLE('',#10337,0.175);
#4755=VERTEX_POINT('',#15896);
#4756=VERTEX_POINT('',#15897);
#4757=VERTEX_POINT('',#15899);
#4758=VERTEX_POINT('',#15901);
#4759=VERTEX_POINT('',#15905);
#4760=VERTEX_POINT('',#15907);
#4761=VERTEX_POINT('',#15911);
#4762=VERTEX_POINT('',#15913);
#4763=VERTEX_POINT('',#15917);
#4764=VERTEX_POINT('',#15919);
#4765=VERTEX_POINT('',#15923);
#4766=VERTEX_POINT('',#15925);
#4767=VERTEX_POINT('',#15933);
#4768=VERTEX_POINT('',#15936);
#4769=VERTEX_POINT('',#15940);
#4770=VERTEX_POINT('',#15944);
#5739=EDGE_CURVE('',#4755,#4756,#3047,.T.);
#5740=EDGE_CURVE('',#4755,#4757,#3048,.T.);
#5741=EDGE_CURVE('',#4757,#4758,#3049,.T.);
#5742=EDGE_CURVE('',#4756,#4758,#3050,.T.);
#5743=EDGE_CURVE('',#4759,#4755,#3051,.T.);
#5744=EDGE_CURVE('',#4759,#4760,#3052,.T.);
#5745=EDGE_CURVE('',#4760,#4757,#3053,.T.);
#5746=EDGE_CURVE('',#4761,#4759,#3054,.T.);
#5747=EDGE_CURVE('',#4761,#4762,#3055,.T.);
#5748=EDGE_CURVE('',#4762,#4760,#3056,.T.);
#5749=EDGE_CURVE('',#4763,#4761,#3057,.T.);
#5750=EDGE_CURVE('',#4763,#4764,#3058,.T.);
#5751=EDGE_CURVE('',#4764,#4762,#3059,.T.);
#5752=EDGE_CURVE('',#4765,#4763,#3060,.T.);
#5753=EDGE_CURVE('',#4765,#4766,#3061,.T.);
#5754=EDGE_CURVE('',#4766,#4764,#3062,.T.);
#5755=EDGE_CURVE('',#4756,#4765,#3063,.T.);
#5756=EDGE_CURVE('',#4758,#4766,#3064,.T.);
#5757=EDGE_CURVE('',#4767,#4767,#4092,.T.);
#5758=EDGE_CURVE('',#4768,#4768,#4093,.T.);
#5759=EDGE_CURVE('',#4768,#4767,#3065,.T.);
#5760=EDGE_CURVE('',#4769,#4769,#4094,.F.);
#5761=EDGE_CURVE('',#4769,#4768,#3066,.T.);
#5762=EDGE_CURVE('',#4770,#4770,#4095,.T.);
#5763=EDGE_CURVE('',#4770,#4769,#3067,.T.);
#7564=ORIENTED_EDGE('',*,*,#5739,.F.);
#7565=ORIENTED_EDGE('',*,*,#5740,.T.);
#7566=ORIENTED_EDGE('',*,*,#5741,.T.);
#7567=ORIENTED_EDGE('',*,*,#5742,.F.);
#7568=ORIENTED_EDGE('',*,*,#5743,.F.);
#7569=ORIENTED_EDGE('',*,*,#5744,.T.);
#7570=ORIENTED_EDGE('',*,*,#5745,.T.);
#7571=ORIENTED_EDGE('',*,*,#5740,.F.);
#7572=ORIENTED_EDGE('',*,*,#5746,.F.);
#7573=ORIENTED_EDGE('',*,*,#5747,.T.);
#7574=ORIENTED_EDGE('',*,*,#5748,.T.);
#7575=ORIENTED_EDGE('',*,*,#5744,.F.);
#7576=ORIENTED_EDGE('',*,*,#5749,.F.);
#7577=ORIENTED_EDGE('',*,*,#5750,.T.);
#7578=ORIENTED_EDGE('',*,*,#5751,.T.);
#7579=ORIENTED_EDGE('',*,*,#5747,.F.);
#7580=ORIENTED_EDGE('',*,*,#5752,.F.);
#7581=ORIENTED_EDGE('',*,*,#5753,.T.);
#7582=ORIENTED_EDGE('',*,*,#5754,.T.);
#7583=ORIENTED_EDGE('',*,*,#5750,.F.);
#7584=ORIENTED_EDGE('',*,*,#5755,.F.);
#7585=ORIENTED_EDGE('',*,*,#5742,.T.);
#7586=ORIENTED_EDGE('',*,*,#5756,.T.);
#7587=ORIENTED_EDGE('',*,*,#5753,.F.);
#7588=ORIENTED_EDGE('',*,*,#5756,.F.);
#7589=ORIENTED_EDGE('',*,*,#5741,.F.);
#7590=ORIENTED_EDGE('',*,*,#5745,.F.);
#7591=ORIENTED_EDGE('',*,*,#5748,.F.);
#7592=ORIENTED_EDGE('',*,*,#5751,.F.);
#7593=ORIENTED_EDGE('',*,*,#5754,.F.);
#7594=ORIENTED_EDGE('',*,*,#5757,.F.);
#7595=ORIENTED_EDGE('',*,*,#5739,.T.);
#7596=ORIENTED_EDGE('',*,*,#5755,.T.);
#7597=ORIENTED_EDGE('',*,*,#5752,.T.);
#7598=ORIENTED_EDGE('',*,*,#5749,.T.);
#7599=ORIENTED_EDGE('',*,*,#5746,.T.);
#7600=ORIENTED_EDGE('',*,*,#5743,.T.);
#7601=ORIENTED_EDGE('',*,*,#5758,.F.);
#7602=ORIENTED_EDGE('',*,*,#5759,.T.);
#7603=ORIENTED_EDGE('',*,*,#5757,.T.);
#7604=ORIENTED_EDGE('',*,*,#5759,.F.);
#7605=ORIENTED_EDGE('',*,*,#5760,.F.);
#7606=ORIENTED_EDGE('',*,*,#5761,.T.);
#7607=ORIENTED_EDGE('',*,*,#5758,.T.);
#7608=ORIENTED_EDGE('',*,*,#5761,.F.);
#7609=ORIENTED_EDGE('',*,*,#5762,.F.);
#7610=ORIENTED_EDGE('',*,*,#5763,.T.);
#7611=ORIENTED_EDGE('',*,*,#5760,.T.);
#7612=ORIENTED_EDGE('',*,*,#5763,.F.);
#7613=ORIENTED_EDGE('',*,*,#5762,.T.);
#8448=CYLINDRICAL_SURFACE('',#10334,0.24505);
#8857=ADVANCED_FACE('',(#1666),#1221,.F.);
#8858=ADVANCED_FACE('',(#1667),#1222,.F.);
#8859=ADVANCED_FACE('',(#1668),#1223,.F.);
#8860=ADVANCED_FACE('',(#1669),#1224,.F.);
#8861=ADVANCED_FACE('',(#1670),#1225,.F.);
#8862=ADVANCED_FACE('',(#1671),#1226,.F.);
#8863=ADVANCED_FACE('',(#1672),#1227,.F.);
#8864=ADVANCED_FACE('',(#1673,#930),#1228,.T.);
#8865=ADVANCED_FACE('',(#1674),#550,.T.);
#8866=ADVANCED_FACE('',(#1675),#8448,.T.);
#8867=ADVANCED_FACE('',(#1676),#551,.T.);
#8868=ADVANCED_FACE('',(#1677),#1229,.T.);
#9082=CLOSED_SHELL('',(#8857,#8858,#8859,#8860,#8861,#8862,#8863,#8864,
#8865,#8866,#8867,#8868));
#10322=AXIS2_PLACEMENT_3D('',#15894,#12535,#12536);
#10323=AXIS2_PLACEMENT_3D('',#15895,#12537,#12538);
#10324=AXIS2_PLACEMENT_3D('',#15904,#12543,#12544);
#10325=AXIS2_PLACEMENT_3D('',#15910,#12548,#12549);
#10326=AXIS2_PLACEMENT_3D('',#15916,#12553,#12554);
#10327=AXIS2_PLACEMENT_3D('',#15922,#12558,#12559);
#10328=AXIS2_PLACEMENT_3D('',#15928,#12563,#12564);
#10329=AXIS2_PLACEMENT_3D('',#15931,#12567,#12568);
#10330=AXIS2_PLACEMENT_3D('',#15932,#12569,#12570);
#10331=AXIS2_PLACEMENT_3D('',#15934,#12571,#12572);
#10332=AXIS2_PLACEMENT_3D('',#15935,#12573,#12574);
#10333=AXIS2_PLACEMENT_3D('',#15937,#12575,#12576);
#10334=AXIS2_PLACEMENT_3D('',#15939,#12578,#12579);
#10335=AXIS2_PLACEMENT_3D('',#15941,#12580,#12581);
#10336=AXIS2_PLACEMENT_3D('',#15943,#12583,#12584);
#10337=AXIS2_PLACEMENT_3D('',#15945,#12585,#12586);
#10338=AXIS2_PLACEMENT_3D('',#15947,#12588,#12589);
#12535=DIRECTION('axis',(0.,0.,1.));
#12536=DIRECTION('refdir',(1.,0.,0.));
#12537=DIRECTION('center_axis',(0.866025403784439,0.,-0.5));
#12538=DIRECTION('ref_axis',(0.5,0.,0.866025403784439));
#12539=DIRECTION('',(0.5,0.,0.866025403784439));
#12540=DIRECTION('',(0.,-1.,0.));
#12541=DIRECTION('',(0.5,0.,0.866025403784439));
#12542=DIRECTION('',(0.,-1.,0.));
#12543=DIRECTION('center_axis',(1.92296268638356E-16,0.,-1.));
#12544=DIRECTION('ref_axis',(1.,0.,1.92296268638356E-16));
#12545=DIRECTION('',(1.,0.,1.92296268638356E-16));
#12546=DIRECTION('',(0.,-1.,0.));
#12547=DIRECTION('',(1.,0.,1.92296268638356E-16));
#12548=DIRECTION('center_axis',(-0.866025403784439,0.,-0.5));
#12549=DIRECTION('ref_axis',(0.5,0.,-0.866025403784439));
#12550=DIRECTION('',(0.5,0.,-0.866025403784439));
#12551=DIRECTION('',(0.,-1.,0.));
#12552=DIRECTION('',(0.5,0.,-0.866025403784438));
#12553=DIRECTION('center_axis',(-0.866025403784439,0.,0.5));
#12554=DIRECTION('ref_axis',(-0.5,0.,-0.866025403784439));
#12555=DIRECTION('',(-0.5,0.,-0.866025403784439));
#12556=DIRECTION('',(0.,-1.,0.));
#12557=DIRECTION('',(-0.5,0.,-0.866025403784439));
#12558=DIRECTION('center_axis',(-1.92296268638356E-16,0.,1.));
#12559=DIRECTION('ref_axis',(-1.,0.,-1.92296268638356E-16));
#12560=DIRECTION('',(-1.,0.,-1.92296268638356E-16));
#12561=DIRECTION('',(0.,-1.,0.));
#12562=DIRECTION('',(-1.,0.,-1.92296268638356E-16));
#12563=DIRECTION('center_axis',(0.866025403784439,0.,0.5));
#12564=DIRECTION('ref_axis',(-0.5,0.,0.866025403784439));
#12565=DIRECTION('',(-0.5,0.,0.866025403784439));
#12566=DIRECTION('',(-0.5,0.,0.866025403784439));
#12567=DIRECTION('center_axis',(0.,-1.,0.));
#12568=DIRECTION('ref_axis',(0.,0.,-1.));
#12569=DIRECTION('center_axis',(0.,1.,0.));
#12570=DIRECTION('ref_axis',(0.,0.,1.));
#12571=DIRECTION('center_axis',(0.,-1.,0.));
#12572=DIRECTION('ref_axis',(1.,0.,0.));
#12573=DIRECTION('center_axis',(0.,-1.,0.));
#12574=DIRECTION('ref_axis',(1.,0.,0.));
#12575=DIRECTION('center_axis',(0.,-1.,0.));
#12576=DIRECTION('ref_axis',(1.,0.,0.));
#12577=DIRECTION('',(0.707106781186547,0.707106781186548,8.65956056235493E-17));
#12578=DIRECTION('center_axis',(0.,-1.,0.));
#12579=DIRECTION('ref_axis',(1.,0.,0.));
#12580=DIRECTION('center_axis',(0.,1.,0.));
#12581=DIRECTION('ref_axis',(1.,0.,0.));
#12582=DIRECTION('',(0.,1.,0.));
#12583=DIRECTION('center_axis',(0.,1.,0.));
#12584=DIRECTION('ref_axis',(1.,0.,0.));
#12585=DIRECTION('center_axis',(0.,-1.,0.));
#12586=DIRECTION('ref_axis',(1.,0.,0.));
#12587=DIRECTION('',(-0.707106781186547,0.707106781186548,-8.65956056235493E-17));
#12588=DIRECTION('center_axis',(0.,-1.,0.));
#12589=DIRECTION('ref_axis',(0.,0.,-1.));
#15894=CARTESIAN_POINT('',(0.,0.,0.));
#15895=CARTESIAN_POINT('Origin',(0.0721687836487032,0.,-0.125));
#15896=CARTESIAN_POINT('',(0.0721687836487032,0.,-0.125));
#15897=CARTESIAN_POINT('',(0.144337567297406,0.,0.));
#15898=CARTESIAN_POINT('',(0.117710979560879,0.,-0.0461186027918559));
#15899=CARTESIAN_POINT('',(0.0721687836487032,-0.25,-0.125));
#15900=CARTESIAN_POINT('',(0.0721687836487032,0.,-0.125));
#15901=CARTESIAN_POINT('',(0.144337567297406,-0.25,0.));
#15902=CARTESIAN_POINT('',(0.144337567297406,-0.25,0.));
#15903=CARTESIAN_POINT('',(0.144337567297406,0.,0.));
#15904=CARTESIAN_POINT('Origin',(-0.0721687836487032,0.,-0.125));
#15905=CARTESIAN_POINT('',(-0.0721687836487032,0.,-0.125));
#15906=CARTESIAN_POINT('',(0.0739156081756484,0.,-0.125));
#15907=CARTESIAN_POINT('',(-0.0721687836487032,-0.25,-0.125));
#15908=CARTESIAN_POINT('',(-0.0721687836487032,0.,-0.125));
#15909=CARTESIAN_POINT('',(0.0721687836487032,-0.25,-0.125));
#15910=CARTESIAN_POINT('Origin',(-0.144337567297406,0.,-4.16333634234434E-17));
#15911=CARTESIAN_POINT('',(-0.144337567297406,0.,-1.76762539787485E-17));
#15912=CARTESIAN_POINT('',(-0.0987953713852306,0.,-0.0788813972081442));
#15913=CARTESIAN_POINT('',(-0.144337567297406,-0.25,-2.77555756156289E-17));
#15914=CARTESIAN_POINT('',(-0.144337567297406,0.,-1.76762539787485E-17));
#15915=CARTESIAN_POINT('',(-0.0721687836487032,-0.25,-0.125));
#15916=CARTESIAN_POINT('Origin',(-0.0721687836487033,0.,0.125));
#15917=CARTESIAN_POINT('',(-0.0721687836487033,0.,0.125));
#15918=CARTESIAN_POINT('',(-0.0627109795608791,0.,0.141381397208144));
#15919=CARTESIAN_POINT('',(-0.0721687836487033,-0.25,0.125));
#15920=CARTESIAN_POINT('',(-0.0721687836487033,0.,0.125));
#15921=CARTESIAN_POINT('',(-0.144337567297406,-0.25,-1.76762539787485E-17));
#15922=CARTESIAN_POINT('Origin',(0.0721687836487032,0.,0.125));
#15923=CARTESIAN_POINT('',(0.0721687836487032,0.,0.125));
#15924=CARTESIAN_POINT('',(0.146084391824352,0.,0.125));
#15925=CARTESIAN_POINT('',(0.0721687836487032,-0.25,0.125));
#15926=CARTESIAN_POINT('',(0.0721687836487032,0.,0.125));
#15927=CARTESIAN_POINT('',(-0.0721687836487033,-0.25,0.125));
#15928=CARTESIAN_POINT('Origin',(0.144337567297406,0.,0.));
#15929=CARTESIAN_POINT('',(0.153795371385231,0.,-0.0163813972081441));
#15930=CARTESIAN_POINT('',(0.0721687836487032,-0.25,0.125));
#15931=CARTESIAN_POINT('Origin',(0.,-0.25,0.));
#15932=CARTESIAN_POINT('Origin',(0.22,0.,0.));
#15933=CARTESIAN_POINT('',(-0.22,-8.67361737988404E-18,-2.69422295812418E-17));
#15934=CARTESIAN_POINT('Origin',(0.,0.,0.));
#15935=CARTESIAN_POINT('Origin',(0.,-0.015,0.));
#15936=CARTESIAN_POINT('',(-0.24505,-0.02505,-3.00099698131059E-17));
#15937=CARTESIAN_POINT('Origin',(0.,-0.02505,0.));
#15938=CARTESIAN_POINT('',(-0.235,-0.015,-2.87791997799628E-17));
#15939=CARTESIAN_POINT('Origin',(0.,-0.3775,0.));
#15940=CARTESIAN_POINT('',(-0.24505,-0.72995,3.00099698131059E-17));
#15941=CARTESIAN_POINT('Origin',(0.,-0.72995,0.));
#15942=CARTESIAN_POINT('',(-0.24505,-0.3775,-3.00099698131059E-17));
#15943=CARTESIAN_POINT('Origin',(0.,-0.7625,0.));
#15944=CARTESIAN_POINT('',(-0.175,-0.8,-2.14313189850787E-17));
#15945=CARTESIAN_POINT('Origin',(0.,-0.8,0.));
#15946=CARTESIAN_POINT('',(-0.2125,-0.7625,-2.60237444818813E-17));
#15947=CARTESIAN_POINT('Origin',(0.,-0.8,0.));
#17236=UNCERTAINTY_MEASURE_WITH_UNIT(LENGTH_MEASURE(0.001),#17323,
'DISTANCE_ACCURACY_VALUE',
'Maximum model space distance between geometric entities at asserted c
onnectivities');
#17261=UNCERTAINTY_MEASURE_WITH_UNIT(LENGTH_MEASURE(0.001),#17323,
'DISTANCE_ACCURACY_VALUE',
'Maximum model space distance between geometric entities at asserted c
onnectivities');
#17297=(
GEOMETRIC_REPRESENTATION_CONTEXT(3)
GLOBAL_UNCERTAINTY_ASSIGNED_CONTEXT((#17236))
GLOBAL_UNIT_ASSIGNED_CONTEXT((#17323,#17325,#17326))
REPRESENTATION_CONTEXT('','3D')
);
#17322=(
GEOMETRIC_REPRESENTATION_CONTEXT(3)
GLOBAL_UNCERTAINTY_ASSIGNED_CONTEXT((#17261))
GLOBAL_UNIT_ASSIGNED_CONTEXT((#17323,#17325,#17326))
REPRESENTATION_CONTEXT('','3D')
);
#17323=(
LENGTH_UNIT()
NAMED_UNIT(*)
SI_UNIT(.CENTI.,.METRE.)
);
#17325=(
NAMED_UNIT(*)
PLANE_ANGLE_UNIT()
SI_UNIT($,.RADIAN.)
);
#17326=(
NAMED_UNIT(*)
SI_UNIT($,.STERADIAN.)
SOLID_ANGLE_UNIT()
);
#17362=SHAPE_DEFINITION_REPRESENTATION(#17424,#17593);
#17424=PRODUCT_DEFINITION_SHAPE('',$,#17654);
#17593=SHAPE_REPRESENTATION('',(#10322),#17297);
#17618=PRODUCT_DEFINITION_CONTEXT('part definition',#17800,'design');
#17654=PRODUCT_DEFINITION('Socket Set Screw - M5x8',
'Socket Set Screw - M5x8',#17714,#17618);
#17714=PRODUCT_DEFINITION_FORMATION('',$,#17837);
#17800=APPLICATION_CONTEXT(
'Core Data for Automotive Mechanical Design Process');
#17801=PRODUCT_CONTEXT('part definition',#17800,'mechanical');
#17837=PRODUCT('Socket Set Screw - M5x8','Socket Set Screw - M5x8',
'Socket Set Screw - M5x8',(#17801));
#17932=COLOUR_RGB('Black',0.12,0.14,0.17);
#17933=FILL_AREA_STYLE_COLOUR('',#17932);
#17934=FILL_AREA_STYLE('',(#17933));
#17935=SURFACE_STYLE_FILL_AREA(#17934);
#17936=SURFACE_SIDE_STYLE('',(#17935));
#17937=SURFACE_STYLE_USAGE(.BOTH.,#17936);
#17938=PRESENTATION_STYLE_ASSIGNMENT((#17937));
ENDSEC;
END-ISO-10303-21;
